ISO-10303-21;
HEADER;
FILE_DESCRIPTION (('STEP AP203'),
    '1' );
FILE_NAME ('oval head_am_B18.6.7M - M2.5 x 0.45 x 20 Type I Cross Recessed OHMS --20C.step',
    '2026-10-08T23:54:15',
    ( '' ),
    ( '' ),
    'SwSTEP 2.0',
    'SolidWorks 2024',
    '' );
FILE_SCHEMA (( 'AUTOMOTIVE_DESIGN' ));
ENDSEC;

DATA;
#189=ORIENTED_EDGE ( 'NONE', *, *, #66768, .T. ) ;
#850=ORIENTED_EDGE ( 'NONE', *, *, #79432, .T. ) ;
#934=CARTESIAN_POINT ( 'NONE',  ( 1.000208336950358934, 2.877919977996279334E-16, -2.349999999999999645 ) ) ;
#1098=CARTESIAN_POINT ( 'NONE',  ( 0.1645010273463769490, 0.3687607960183755251, -1.417169167140624575 ) ) ;
#1268=VECTOR ( 'NONE', #59346, 1000.000000000000114 ) ;
#1298=CARTESIAN_POINT ( 'NONE',  ( 2.246611357655419638, -0.1632191352058106892, -0.1632191352058112721 ) ) ;
#1322=EDGE_CURVE ( 'NONE', #98063, #56695, #34552, .T. ) ;
#1368=CARTESIAN_POINT ( 'NONE',  ( 0.4325450954222598288, 0.000000000000000000, 0.000000000000000000 ) ) ;
#1533=CARTESIAN_POINT ( 'NONE',  ( 0.000000000000000000, 0.000000000000000000, 0.000000000000000000 ) ) ;
#2042=ADVANCED_FACE ( 'NONE', ( #34182 ), #49922, .T. ) ;
#2341=SHAPE_DEFINITION_REPRESENTATION ( #87067, #9419 ) ;
#2377=EDGE_CURVE ( 'NONE', #35831, #18999, #9208, .T. ) ;
#2714=ORIENTED_EDGE ( 'NONE', *, *, #46349, .T. ) ;
#2794=AXIS2_PLACEMENT_3D ( 'NONE', #71261, #56049, #41826 ) ;
#2974=EDGE_LOOP ( 'NONE', ( #28351, #59246, #47547, #91223, #17126 ) ) ;
#3284=EDGE_CURVE ( 'NONE', #12764, #77091, #66299, .T. ) ;
#3599=ORIENTED_EDGE ( 'NONE', *, *, #21854, .F. ) ;
#3776=ORIENTED_EDGE ( 'NONE', *, *, #16769, .T. ) ;
#3778=CARTESIAN_POINT ( 'NONE',  ( 0.000000000000000000, -0.3850000000000046163, 1.529999999999998916 ) ) ;
#3832=CIRCLE ( 'NONE', #47655, 2.349999999999999645 ) ;
#3877=ORIENTED_EDGE ( 'NONE', *, *, #20018, .F. ) ;
#3946=ORIENTED_EDGE ( 'NONE', *, *, #10129, .F. ) ;
#4007=ORIENTED_EDGE ( 'NONE', *, *, #63217, .F. ) ;
#4117=DIRECTION ( 'NONE',  ( -0.9951627101165076983, 0.000000000000000000, 0.09824042138329588947 ) ) ;
#4247=EDGE_CURVE ( 'NONE', #10125, #59687, #57317, .T. ) ;
#4300=CARTESIAN_POINT ( 'NONE',  ( 0.4325450954222598288, 2.349999999999997868, 2.877919977996277362E-16 ) ) ;
#4319=AXIS2_PLACEMENT_3D ( 'NONE', #25092, #26103, #9874 ) ;
#4672=AXIS2_PLACEMENT_3D ( 'NONE', #89717, #49668, #11090 ) ;
#4689=CARTESIAN_POINT ( 'NONE',  ( 5.202077965628057576, 2.038091937962834166, 2.869745073849996442E-16 ) ) ;
#4705=DIRECTION ( 'NONE',  ( 0.000000000000000000, 0.000000000000000000, 1.000000000000000000 ) ) ;
#4885=EDGE_CURVE ( 'NONE', #44866, #18999, #81636, .T. ) ;
#5241=FACE_OUTER_BOUND ( 'NONE', #57390, .T. ) ;
#5594=DIRECTION ( 'NONE',  ( 0.000000000000000000, -1.224646799147353207E-16, 1.000000000000000000 ) ) ;
#5713=AXIS2_PLACEMENT_3D ( 'NONE', #69854, #48022, #40899 ) ;
#5943=CARTESIAN_POINT ( 'NONE',  ( 1.949999999999999956, 0.1924999999999999489, 0.1925000000000000322 ) ) ;
#6040=CIRCLE ( 'NONE', #25528, 6.600000000000001421 ) ;
#6069=VECTOR ( 'NONE', #98615, 1000.000000000000000 ) ;
#6167=CARTESIAN_POINT ( 'NONE',  ( -15.87499999999997868, 1.530808498934188119E-16, -1.249999999999997113 ) ) ;
#6404=FACE_OUTER_BOUND ( 'NONE', #56949, .T. ) ;
#6415=EDGE_CURVE ( 'NONE', #44866, #86377, #93125, .T. ) ;
#6552=LINE ( 'NONE', #38000, #15185 ) ;
#6671=CARTESIAN_POINT ( 'NONE',  ( 5.202077965628057576, 7.402934475628871785E-15, -2.038091937962834166 ) ) ;
#6735=ORIENTED_EDGE ( 'NONE', *, *, #3284, .T. ) ;
#6801=VECTOR ( 'NONE', #28505, 1000.000000000000000 ) ;
#6824=DIRECTION ( 'NONE',  ( -1.000000000000000000, -0.000000000000000000, -0.000000000000000000 ) ) ;
#6880=AXIS2_PLACEMENT_3D ( 'NONE', #78183, #73593, #87818 ) ;
#7377=CONICAL_SURFACE ( 'NONE', #13812, 1.249999999999996003, 0.7853981633974514986 ) ;
#7783=DIRECTION ( 'NONE',  ( -0.9951627101165078093, 0.000000000000000000, 0.09824042138329590335 ) ) ;
#7816=DIRECTION ( 'NONE',  ( 0.9951627101165076983, 0.000000000000000000, 0.09824042138329622254 ) ) ;
#7954=CARTESIAN_POINT ( 'NONE',  ( 2.230654205607476293, -6.505213034913026604E-16, -0.1647943925233646134 ) ) ;
#8014=ORIENTED_EDGE ( 'NONE', *, *, #4247, .T. ) ;
#8243=VERTEX_POINT ( 'NONE', #21492 ) ;
#8247=ORIENTED_EDGE ( 'NONE', *, *, #6415, .T. ) ;
#8393=DIRECTION ( 'NONE',  ( 0.9951627101165076983, -0.09824042138329622254, -3.430045979798646929E-16 ) ) ;
#8521=ORIENTED_EDGE ( 'NONE', *, *, #43858, .F. ) ;
#8639=DIRECTION ( 'NONE',  ( -0.000000000000000000, 0.000000000000000000, 1.000000000000000000 ) ) ;
#8783=FACE_OUTER_BOUND ( 'NONE', #45727, .T. ) ;
#8918=ORIENTED_EDGE ( 'NONE', *, *, #6415, .F. ) ;
#9029=FACE_OUTER_BOUND ( 'NONE', #75515, .T. ) ;
#9157=EDGE_LOOP ( 'NONE', ( #69653, #42715, #67109, #46719, #23121 ) ) ;
#9208=LINE ( 'NONE', #79219, #88920 ) ;
#9419=SHAPE_REPRESENTATION ( 'oval head_am_B18.6.7M - M2.5 x 0.45 x 20 Type I Cross Recessed OHMS --20C', ( #37391 ), #16366 ) ;
#9634=ORIENTED_EDGE ( 'NONE', *, *, #27935, .F. ) ;
#9691=EDGE_CURVE ( 'NONE', #35831, #10125, #97157, .T. ) ;
#9874=DIRECTION ( 'NONE',  ( 0.000000000000000000, 0.000000000000000000, 1.000000000000000000 ) ) ;
#10050=SPHERICAL_SURFACE ( 'NONE', #12943, 6.600000000000001421 ) ;
#10086=DIRECTION ( 'NONE',  ( -1.000000000000000000, -0.000000000000000000, -0.000000000000000000 ) ) ;
#10091=PLANE ( 'NONE',  #30578 ) ;
#10125=VERTEX_POINT ( 'NONE', #53862 ) ;
#10129=EDGE_CURVE ( 'NONE', #29436, #59687, #87899, .T. ) ;
#10598=CARTESIAN_POINT ( 'NONE',  ( 0.4325450954222598288, 2.877919977996279827E-16, -2.350000000000000089 ) ) ;
#11039=AXIS2_PLACEMENT_3D ( 'NONE', #45820, #54937, #23451 ) ;
#11090=DIRECTION ( 'NONE',  ( -0.8246584009594636333, -1.974890369949422540E-15, 0.5656310827093757876 ) ) ;
#11120=AXIS2_PLACEMENT_3D ( 'NONE', #19937, #42804, #95572 ) ;
#11133=ORIENTED_EDGE ( 'NONE', *, *, #49549, .T. ) ;
#11244=EDGE_LOOP ( 'NONE', ( #59487, #28475, #64691, #63639, #78523 ) ) ;
#11376=LINE ( 'NONE', #3778, #93663 ) ;
#11559=CARTESIAN_POINT ( 'NONE',  ( 0.1645010273463760886, 1.417169167140627462, -0.3687607960183705846 ) ) ;
#11694=VERTEX_POINT ( 'NONE', #11559 ) ;
#11712=FACE_OUTER_BOUND ( 'NONE', #16184, .T. ) ;
#11832=ADVANCED_FACE ( 'NONE', ( #75444 ), #83055, .F. ) ;
#11905=EDGE_CURVE ( 'NONE', #52201, #11694, #42973, .T. ) ;
#11916=CARTESIAN_POINT ( 'NONE',  ( 2.246611357655420083, 0.1632191352058106337, 0.1632191352058112166 ) ) ;
#11976=CARTESIAN_POINT ( 'NONE',  ( 5.202077965628057576, -7.402934475628873363E-15, 2.038091937962834166 ) ) ;
#12361=ORIENTED_EDGE ( 'NONE', *, *, #71364, .F. ) ;
#12449=CARTESIAN_POINT ( 'NONE',  ( 1.949999999999999956, -0.1925000000000001155, -0.1925000000000000600 ) ) ;
#12694=CIRCLE ( 'NONE', #95347, 6.600000000000001421 ) ;
#12748=VECTOR ( 'NONE', #74849, 1000.000000000000227 ) ;
#12764=VERTEX_POINT ( 'NONE', #1098 ) ;
#12795=CARTESIAN_POINT ( 'NONE',  ( 1.000208336950358934, 0.000000000000000000, 0.000000000000000000 ) ) ;
#12902=DIRECTION ( 'NONE',  ( -0.9903949459893287566, 0.09776975748868974025, 0.09776975748868974025 ) ) ;
#12943=AXIS2_PLACEMENT_3D ( 'NONE', #40515, #54243, #24764 ) ;
#12948=DIRECTION ( 'NONE',  ( -1.000000000000000000, -0.000000000000000000, -0.000000000000000000 ) ) ;
#12949=LINE ( 'NONE', #52527, #12748 ) ;
#13326=ADVANCED_FACE ( 'NONE', ( #49176 ), #7377, .T. ) ;
#13439=CIRCLE ( 'NONE', #42670, 6.594667762285751245 ) ;
#13812=AXIS2_PLACEMENT_3D ( 'NONE', #41048, #12948, #33423 ) ;
#14113=PRODUCT_DEFINITION ( 'UNKNOWN', '', #47237, #43907 ) ;
#14268=ADVANCED_FACE ( 'NONE', ( #11712 ), #25947, .T. ) ;
#14273=ADVANCED_FACE ( 'NONE', ( #79725 ), #57421, .T. ) ;
#14390=DIRECTION ( 'NONE',  ( 0.09824042138329590335, -4.470611911092166224E-17, 0.9951627101165079203 ) ) ;
#15185=VECTOR ( 'NONE', #30885, 999.9999999999998863 ) ;
#15387=DIRECTION ( 'NONE',  ( 0.8219392559241307517, -0.5637660281018076480, -0.08114015731558694988 ) ) ;
#15467=DIRECTION ( 'NONE',  ( 0.8246584009594635223, 0.5656310827093757876, 0.000000000000000000 ) ) ;
#15782=DIRECTION ( 'NONE',  ( -0.5656310827093757876, 2.995395837334947896E-15, -0.8246584009594636333 ) ) ;
#15813=ORIENTED_EDGE ( 'NONE', *, *, #78206, .T. ) ;
#16118=CARTESIAN_POINT ( 'NONE',  ( 0.000000000000000000, 1.530000000000000027, -0.3849999999999998979 ) ) ;
#16184=EDGE_LOOP ( 'NONE', ( #9634, #90032, #65325 ) ) ;
#16196=CARTESIAN_POINT ( 'NONE',  ( 2.230654205607476293, 0.1647943925233646134, -7.514475724998474108E-17 ) ) ;
#16244=DIRECTION ( 'NONE',  ( -1.000000000000000000, 0.000000000000000000, -0.000000000000000000 ) ) ;
#16366=( GEOMETRIC_REPRESENTATION_CONTEXT ( 3 ) GLOBAL_UNCERTAINTY_ASSIGNED_CONTEXT ( ( #34800 ) ) GLOBAL_UNIT_ASSIGNED_CONTEXT ( ( #79474, #81347, #89461 ) ) REPRESENTATION_CONTEXT ( 'NONE', 'WORKASPACE' ) );
#16382=CARTESIAN_POINT ( 'NONE',  ( 1.949999999999999956, 0.1925000000000007538, -0.1924999999999994493 ) ) ;
#16462=LINE ( 'NONE', #85988, #64101 ) ;
#16769=EDGE_CURVE ( 'NONE', #36724, #49066, #86655, .T. ) ;
#17126=ORIENTED_EDGE ( 'NONE', *, *, #66768, .F. ) ;
#17305=AXIS2_PLACEMENT_3D ( 'NONE', #83912, #14390, #7783 ) ;
#17831=AXIS2_PLACEMENT_3D ( 'NONE', #54421, #90980, #83863 ) ;
#17924=CARTESIAN_POINT ( 'NONE',  ( 0.1645010273463760886, -0.3687607960183749145, 1.417169167140625907 ) ) ;
#17955=ORIENTED_EDGE ( 'NONE', *, *, #37866, .F. ) ;
#18152=DIRECTION ( 'NONE',  ( 0.000000000000000000, -1.000000000000000000, 0.000000000000000000 ) ) ;
#18361=ORIENTED_EDGE ( 'NONE', *, *, #90534, .T. ) ;
#18442=EDGE_CURVE ( 'NONE', #72919, #45742, #94970, .T. ) ;
#18488=CYLINDRICAL_SURFACE ( 'NONE', #4319, 2.349999999999999645 ) ;
#18921=VERTEX_POINT ( 'NONE', #29548 ) ;
#18968=EDGE_CURVE ( 'NONE', #45742, #72919, #56179, .T. ) ;
#18999=VERTEX_POINT ( 'NONE', #38153 ) ;
#19090=ORIENTED_EDGE ( 'NONE', *, *, #70339, .T. ) ;
#19308=CARTESIAN_POINT ( 'NONE',  ( 6.573941812937369455, 0.2639660507643281639, 9.334907998774166978E-16 ) ) ;
#19310=DIRECTION ( 'NONE',  ( 0.8219392559241307517, 0.5637660281018075370, -0.08114015731558690825 ) ) ;
#19563=DIRECTION ( 'NONE',  ( -1.000000000000000000, -0.000000000000000000, -0.000000000000000000 ) ) ;
#19679=CARTESIAN_POINT ( 'NONE',  ( 1.949999999999999956, -0.1925000000000001710, 0.1924999999999999212 ) ) ;
#19716=CARTESIAN_POINT ( 'NONE',  ( 1.949999999999999956, -0.1925000000000001155, -0.1925000000000000600 ) ) ;
#19916=AXIS2_PLACEMENT_3D ( 'NONE', #46375, #78311, #39754 ) ;
#19937=CARTESIAN_POINT ( 'NONE',  ( 2.230654205607476737, -0.1647943925233645579, -7.922169807384186089E-16 ) ) ;
#20018=EDGE_CURVE ( 'NONE', #12764, #18999, #63799, .T. ) ;
#20263=ADVANCED_FACE ( 'NONE', ( #41312 ), #94590, .T. ) ;
#20499=ORIENTED_EDGE ( 'NONE', *, *, #96962, .T. ) ;
#20559=VECTOR ( 'NONE', #15387, 999.9999999999998863 ) ;
#20677=CARTESIAN_POINT ( 'NONE',  ( 6.573941812937369455, -7.905506363763796338E-18, 0.2639660507643297183 ) ) ;
#21228=CARTESIAN_POINT ( 'NONE',  ( 0.1553305729023591875, 1.423459158329793306, 1.743234701965566823E-16 ) ) ;
#21492=CARTESIAN_POINT ( 'NONE',  ( 0.4325450954222598288, -2.349999999999997868, 0.000000000000000000 ) ) ;
#21614=EDGE_CURVE ( 'NONE', #29436, #56695, #11376, .T. ) ;
#21854=EDGE_CURVE ( 'NONE', #29476, #93240, #45017, .T. ) ;
#21939=DIRECTION ( 'NONE',  ( -0.09824042138329623641, -2.980407940728110405E-17, 0.9951627101165078093 ) ) ;
#21943=CARTESIAN_POINT ( 'NONE',  ( -15.87499999999997868, 0.000000000000000000, 1.249999999999997113 ) ) ;
#22394=VECTOR ( 'NONE', #19310, 1000.000000000000114 ) ;
#22442=LINE ( 'NONE', #21943, #46051 ) ;
#22601=DIRECTION ( 'NONE',  ( 0.000000000000000000, -1.408054769461694189E-16, 1.000000000000000000 ) ) ;
#22870=LINE ( 'NONE', #6167, #86805 ) ;
#23121=ORIENTED_EDGE ( 'NONE', *, *, #27927, .F. ) ;
#23150=DIRECTION ( 'NONE',  ( -0.8246584009594636333, 0.5656310827093757876, 0.000000000000000000 ) ) ;
#23238=ORIENTED_EDGE ( 'NONE', *, *, #96962, .F. ) ;
#23272=APPLICATION_CONTEXT ( 'configuration controlled 3d designs of mechanical parts and assemblies' ) ;
#23448=ADVANCED_FACE ( 'NONE', ( #5241 ), #29073, .T. ) ;
#23451=DIRECTION ( 'NONE',  ( 0.000000000000000000, 0.000000000000000000, 1.000000000000000000 ) ) ;
#23542=AXIS2_PLACEMENT_3D ( 'NONE', #91464, #21939, #36200 ) ;
#23729=LINE ( 'NONE', #16118, #37750 ) ;
#23823=CARTESIAN_POINT ( 'NONE',  ( 0.02224039135773590858, 0.3828044741864812250, -0.3828044741864797817 ) ) ;
#23840=VECTOR ( 'NONE', #56174, 1000.000000000000114 ) ;
#23848=EDGE_LOOP ( 'NONE', ( #39851, #35387, #85907 ) ) ;
#23849=CARTESIAN_POINT ( 'NONE',  ( 20.60020833695035236, 0.000000000000000000, 0.000000000000000000 ) ) ;
#24199=CIRCLE ( 'NONE', #50151, 6.594667762285751245 ) ;
#24303=ORIENTED_EDGE ( 'NONE', *, *, #59414, .F. ) ;
#24342=VECTOR ( 'NONE', #77040, 1000.000000000000000 ) ;
#24629=EDGE_LOOP ( 'NONE', ( #71403, #4007, #23238 ) ) ;
#24764=DIRECTION ( 'NONE',  ( 0.000000000000000000, -1.000000000000000000, 0.000000000000000000 ) ) ;
#24854=DIRECTION ( 'NONE',  ( 1.000000000000000000, 0.000000000000000000, 0.000000000000000000 ) ) ;
#25092=CARTESIAN_POINT ( 'NONE',  ( -15.87499999999997868, 0.000000000000000000, 0.000000000000000000 ) ) ;
#25198=CARTESIAN_POINT ( 'NONE',  ( 0.000000000000000000, 0.3850000000000053935, -1.529999999999998916 ) ) ;
#25313=FACE_OUTER_BOUND ( 'NONE', #24629, .T. ) ;
#25479=ADVANCED_FACE ( 'NONE', ( #25625 ), #56597, .T. ) ;
#25528=AXIS2_PLACEMENT_3D ( 'NONE', #66729, #29626, #60602 ) ;
#25625=FACE_OUTER_BOUND ( 'NONE', #30110, .T. ) ;
#25947=PLANE ( 'NONE',  #54358 ) ;
#26103=DIRECTION ( 'NONE',  ( -1.000000000000000000, -0.000000000000000000, -0.000000000000000000 ) ) ;
#26457=CARTESIAN_POINT ( 'NONE',  ( 2.230654205607476737, -2.168404344971008868E-16, 0.1647943925233645579 ) ) ;
#26518=AXIS2_PLACEMENT_3D ( 'NONE', #93309, #10086, #48672 ) ;
#26632=DIRECTION ( 'NONE',  ( -0.09824042138329590335, 0.9951627101165078093, 3.519298150595267489E-15 ) ) ;
#26653=EDGE_CURVE ( 'NONE', #59687, #35831, #91007, .T. ) ;
#27386=ORIENTED_EDGE ( 'NONE', *, *, #18442, .F. ) ;
#27634=DIRECTION ( 'NONE',  ( -0.9951627101165076983, -0.09824042138329588947, -3.430045979798635096E-16 ) ) ;
#27812=FACE_OUTER_BOUND ( 'NONE', #90978, .T. ) ;
#27927=EDGE_CURVE ( 'NONE', #18921, #35831, #46350, .T. ) ;
#27935=EDGE_CURVE ( 'NONE', #41575, #98063, #44917, .T. ) ;
#27995=VECTOR ( 'NONE', #12902, 1000.000000000000227 ) ;
#28351=ORIENTED_EDGE ( 'NONE', *, *, #81227, .T. ) ;
#28475=ORIENTED_EDGE ( 'NONE', *, *, #59414, .T. ) ;
#28505=DIRECTION ( 'NONE',  ( 0.000000000000000000, -1.000000000000000000, -2.816109538923387391E-16 ) ) ;
#28832=PRODUCT ( 'oval head_am_B18.6.7M - M2.5 x 0.45 x 20 Type I Cross Recessed OHMS --20C', 'oval head_am_B18.6.7M - M2.5 x 0.45 x 20 Type I Cross Recessed OHMS --20C', '', ( #46012 ) ) ;
#28963=AXIS2_PLACEMENT_3D ( 'NONE', #58233, #74920, #90658 ) ;
#29073=PLANE ( 'NONE',  #23542 ) ;
#29075=DIRECTION ( 'NONE',  ( -1.000000000000000000, -0.000000000000000000, -0.000000000000000000 ) ) ;
#29436=VERTEX_POINT ( 'NONE', #17924 ) ;
#29476=VERTEX_POINT ( 'NONE', #81318 ) ;
#29505=DIRECTION ( 'NONE',  ( 0.8246584009594635223, 1.154631945610162960E-14, -0.5656310827093757876 ) ) ;
#29548=CARTESIAN_POINT ( 'NONE',  ( 0.1645010273463760886, 1.417169167140627906, 0.3687607960183699740 ) ) ;
#29591=ORIENTED_EDGE ( 'NONE', *, *, #58050, .T. ) ;
#29626=DIRECTION ( 'NONE',  ( 0.000000000000000000, 0.000000000000000000, -1.000000000000000000 ) ) ;
#29912=AXIS2_PLACEMENT_3D ( 'NONE', #5943, #98787, #23150 ) ;
#30110=EDGE_LOOP ( 'NONE', ( #8918, #96239, #42220 ) ) ;
#30113=ADVANCED_FACE ( 'NONE', ( #6404 ), #53593, .T. ) ;
#30226=DIRECTION ( 'NONE',  ( -0.09824042138329623641, -0.9951627101165078093, -3.504396110891626425E-15 ) ) ;
#30578=AXIS2_PLACEMENT_3D ( 'NONE', #16196, #77586, #54782 ) ;
#30789=AXIS2_PLACEMENT_3D ( 'NONE', #16382, #39721, #40236 ) ;
#30865=VECTOR ( 'NONE', #72432, 1000.000000000000000 ) ;
#30885=DIRECTION ( 'NONE',  ( 0.8219392559241307517, 0.08114015731558495148, 0.5637660281018078701 ) ) ;
#31126=ORIENTED_EDGE ( 'NONE', *, *, #45417, .T. ) ;
#31435=VERTEX_POINT ( 'NONE', #34908 ) ;
#32366=CARTESIAN_POINT ( 'NONE',  ( 2.230654205607476737, -2.168404344971008868E-16, 0.1647943925233645579 ) ) ;
#32621=ORIENTED_EDGE ( 'NONE', *, *, #94899, .F. ) ;
#32876=DIRECTION ( 'NONE',  ( -0.09824042138329590335, 4.470611911092166224E-17, -0.9951627101165078093 ) ) ;
#32968=EDGE_LOOP ( 'NONE', ( #50939, #850, #58038, #65121 ) ) ;
#33068=ORIENTED_EDGE ( 'NONE', *, *, #72028, .F. ) ;
#33189=DIRECTION ( 'NONE',  ( 0.000000000000000000, 0.000000000000000000, 1.000000000000000000 ) ) ;
#33269=AXIS2_PLACEMENT_3D ( 'NONE', #80233, #35067, #96457 ) ;
#33423=DIRECTION ( 'NONE',  ( 0.000000000000000000, 0.000000000000000000, 1.000000000000000000 ) ) ;
#33426=PLANE ( 'NONE',  #4672 ) ;
#33439=DIRECTION ( 'NONE',  ( -0.7071067811865452413, 8.659560562354961208E-17, -0.7071067811865497932 ) ) ;
#33536=EDGE_LOOP ( 'NONE', ( #40142, #3776, #78587, #73491, #19090, #8014, #3946, #56191, #53906, #36524, #93062 ) ) ;
#33966=AXIS2_PLACEMENT_3D ( 'NONE', #89179, #65867, #34895 ) ;
#34047=ADVANCED_FACE ( 'NONE', ( #54742 ), #10050, .T. ) ;
#34182=FACE_OUTER_BOUND ( 'NONE', #23848, .T. ) ;
#34187=EDGE_CURVE ( 'NONE', #18921, #52201, #71263, .T. ) ;
#34267=APPLICATION_CONTEXT ( 'configuration controlled 3d designs of mechanical parts and assemblies' ) ;
#34552=LINE ( 'NONE', #57903, #22394 ) ;
#34800=UNCERTAINTY_MEASURE_WITH_UNIT (LENGTH_MEASURE( 1.000000000000000082E-05 ), #79474, 'distance_accuracy_value', 'NONE');
#34895=DIRECTION ( 'NONE',  ( -0.8246584009594635223, 0.5656310827093757876, 1.065814103640150279E-14 ) ) ;
#34908=CARTESIAN_POINT ( 'NONE',  ( 0.1553305729023591875, -1.423459158329792640, 2.407412430484044816E-32 ) ) ;
#34963=DIRECTION ( 'NONE',  ( 0.000000000000000000, 1.000000000000000000, 0.000000000000000000 ) ) ;
#35009=CIRCLE ( 'NONE', #47979, 1.249999999999996003 ) ;
#35067=DIRECTION ( 'NONE',  ( -1.000000000000000000, 0.000000000000000000, 0.000000000000000000 ) ) ;
#35387=ORIENTED_EDGE ( 'NONE', *, *, #95823, .F. ) ;
#35559=CARTESIAN_POINT ( 'NONE',  ( 6.600000000000001421, 0.000000000000000000, 0.000000000000000000 ) ) ;
#35831=VERTEX_POINT ( 'NONE', #44971 ) ;
#35941=DIRECTION ( 'NONE',  ( 0.9951627101165076983, -0.09824042138329622254, -8.881784197001249168E-15 ) ) ;
#36037=DIRECTION ( 'NONE',  ( 0.09824042138329590335, -0.9951627101165079203, -3.519298150595267883E-15 ) ) ;
#36200=DIRECTION ( 'NONE',  ( 0.9951627101165076983, 0.000000000000000000, 0.09824042138329622254 ) ) ;
#36326=EDGE_LOOP ( 'NONE', ( #78371, #55106, #17955 ) ) ;
#36339=VECTOR ( 'NONE', #33439, 1000.000000000000000 ) ;
#36524=ORIENTED_EDGE ( 'NONE', *, *, #46363, .F. ) ;
#36662=AXIS2_PLACEMENT_3D ( 'NONE', #23849, #16244, #8639 ) ;
#36669=AXIS2_PLACEMENT_3D ( 'NONE', #37170, #53404, #45782 ) ;
#36724=VERTEX_POINT ( 'NONE', #57582 ) ;
#37170=CARTESIAN_POINT ( 'NONE',  ( 20.60020833695035236, 0.000000000000000000, 0.000000000000000000 ) ) ;
#37294=ADVANCED_FACE ( 'NONE', ( #9029 ), #40988, .T. ) ;
#37391=AXIS2_PLACEMENT_3D ( 'NONE', #1533, #63447, #24854 ) ;
#37750=VECTOR ( 'NONE', #54207, 1000.000000000000000 ) ;
#37866=EDGE_CURVE ( 'NONE', #11694, #18999, #23729, .T. ) ;
#38000=CARTESIAN_POINT ( 'NONE',  ( 0.000000000000000000, -0.3849999999999936806, -1.530000000000001359 ) ) ;
#38042=CYLINDRICAL_SURFACE ( 'NONE', #64165, 2.349999999999999645 ) ;
#38153=CARTESIAN_POINT ( 'NONE',  ( 1.949999999999999956, 0.1925000000000007538, -0.1924999999999994493 ) ) ;
#38357=ORIENTED_EDGE ( 'NONE', *, *, #40541, .T. ) ;
#38654=ADVANCED_FACE ( 'NONE', ( #57732 ), #49125, .T. ) ;
#38806=DIRECTION ( 'NONE',  ( -0.5656310827093756766, 0.8246584009594636333, 1.161164194647626880E-16 ) ) ;
#39348=DIRECTION ( 'NONE',  ( -0.9903949459893287566, -0.09776975748868939331, -0.09776975748869010108 ) ) ;
#39477=AXIS2_PLACEMENT_3D ( 'NONE', #98202, #59166, #43936 ) ;
#39721=DIRECTION ( 'NONE',  ( 0.5656310827093757876, 2.995395837334948684E-15, -0.8246584009594636333 ) ) ;
#39754=DIRECTION ( 'NONE',  ( 0.000000000000000000, 0.000000000000000000, 1.000000000000000000 ) ) ;
#39851=ORIENTED_EDGE ( 'NONE', *, *, #21614, .T. ) ;
#40142=ORIENTED_EDGE ( 'NONE', *, *, #76912, .T. ) ;
#40236=DIRECTION ( 'NONE',  ( 0.8246584009594636333, -1.974890369949422146E-15, 0.5656310827093757876 ) ) ;
#40515=CARTESIAN_POINT ( 'NONE',  ( 6.600000000000001421, 0.000000000000000000, 0.000000000000000000 ) ) ;
#40541=EDGE_CURVE ( 'NONE', #49066, #53606, #50873, .T. ) ;
#40899=DIRECTION ( 'NONE',  ( -0.8246584009594635223, 0.5656310827093757876, 0.000000000000000000 ) ) ;
#40902=DIRECTION ( 'NONE',  ( 0.000000000000000000, 0.000000000000000000, 1.000000000000000000 ) ) ;
#40917=DIRECTION ( 'NONE',  ( 0.000000000000000000, 0.000000000000000000, 1.000000000000000000 ) ) ;
#40925=CIRCLE ( 'NONE', #6880, 2.350000000000000089 ) ;
#40967=ORIENTED_EDGE ( 'NONE', *, *, #58050, .F. ) ;
#40988=PLANE ( 'NONE',  #55511 ) ;
#41048=CARTESIAN_POINT ( 'NONE',  ( 2.100208336950355914, 0.000000000000000000, 0.000000000000000000 ) ) ;
#41312=FACE_OUTER_BOUND ( 'NONE', #85867, .T. ) ;
#41575=VERTEX_POINT ( 'NONE', #79460 ) ;
#41826=DIRECTION ( 'NONE',  ( 0.000000000000000000, 0.000000000000000000, 1.000000000000000000 ) ) ;
#42220=ORIENTED_EDGE ( 'NONE', *, *, #78206, .F. ) ;
#42224=EDGE_LOOP ( 'NONE', ( #67507, #29591, #32621, #80947 ) ) ;
#42350=EDGE_LOOP ( 'NONE', ( #89019, #11133, #88497, #12361 ) ) ;
#42411=MANIFOLD_SOLID_BREP ( 'CirPattern1', #43583 ) ;
#42499=ORIENTED_EDGE ( 'NONE', *, *, #27927, .T. ) ;
#42574=CARTESIAN_POINT ( 'NONE',  ( 6.573941812937369455, -0.2639660507643297183, -9.295380466955404257E-16 ) ) ;
#42670=AXIS2_PLACEMENT_3D ( 'NONE', #20677, #56901, #87835 ) ;
#42715=ORIENTED_EDGE ( 'NONE', *, *, #11905, .T. ) ;
#42803=DIRECTION ( 'NONE',  ( -1.000000000000000000, -0.000000000000000000, -0.000000000000000000 ) ) ;
#42804=DIRECTION ( 'NONE',  ( -0.09824042138329590335, 0.9951627101165078093, 3.519298150595267489E-15 ) ) ;
#42973=CIRCLE ( 'NONE', #5713, 6.119803529381342422 ) ;
#43443=DIRECTION ( 'NONE',  ( -0.8246584009594636333, 0.000000000000000000, -0.5656310827093756766 ) ) ;
#43583=CLOSED_SHELL ( 'NONE', ( #78306, #95076, #59944, #38654, #34047, #75319, #23448, #37294, #14268, #93958, #67830, #13326, #20263, #14273, #11832, #75509, #30113, #2042, #64988, #64703, #25479, #89774 ) ) ;
#43858=EDGE_CURVE ( 'NONE', #76458, #86377, #71764, .T. ) ;
#43907=DESIGN_CONTEXT ( 'detailed design', #23272, 'design' ) ;
#43936=DIRECTION ( 'NONE',  ( 0.9951627101165076983, -0.09824042138329622254, 0.000000000000000000 ) ) ;
#43967=ORIENTED_EDGE ( 'NONE', *, *, #81227, .F. ) ;
#44426=EDGE_CURVE ( 'NONE', #96655, #11694, #13439, .T. ) ;
#44866=VERTEX_POINT ( 'NONE', #12449 ) ;
#44917=CIRCLE ( 'NONE', #17305, 6.594667762285749468 ) ;
#44971=CARTESIAN_POINT ( 'NONE',  ( 1.949999999999999734, 0.1924999999999993938, 0.1925000000000007261 ) ) ;
#45017=CIRCLE ( 'NONE', #11039, 1.249999999999996003 ) ;
#45406=FACE_OUTER_BOUND ( 'NONE', #42350, .T. ) ;
#45417=EDGE_CURVE ( 'NONE', #77091, #44866, #6552, .T. ) ;
#45663=DIRECTION ( 'NONE',  ( 0.000000000000000000, 0.000000000000000000, 1.000000000000000000 ) ) ;
#45727=EDGE_LOOP ( 'NONE', ( #6735, #31126, #50960, #3877 ) ) ;
#45742=VERTEX_POINT ( 'NONE', #96288 ) ;
#45782=DIRECTION ( 'NONE',  ( 0.000000000000000000, 0.000000000000000000, 1.000000000000000000 ) ) ;
#45820=CARTESIAN_POINT ( 'NONE',  ( 2.100208336950355914, 0.000000000000000000, 0.000000000000000000 ) ) ;
#45941=CARTESIAN_POINT ( 'NONE',  ( 1.000208336950358934, 0.000000000000000000, 0.000000000000000000 ) ) ;
#46012=MECHANICAL_CONTEXT ( 'NONE', #34267, 'mechanical' ) ;
#46051=VECTOR ( 'NONE', #29075, 1000.000000000000000 ) ;
#46113=CARTESIAN_POINT ( 'NONE',  ( -15.87499999999997868, 0.000000000000000000, 2.349999999999999645 ) ) ;
#46346=ORIENTED_EDGE ( 'NONE', *, *, #18442, .T. ) ;
#46349=EDGE_CURVE ( 'NONE', #87941, #71994, #3832, .T. ) ;
#46350=LINE ( 'NONE', #52976, #20559 ) ;
#46363=EDGE_CURVE ( 'NONE', #31435, #98063, #93031, .T. ) ;
#46375=CARTESIAN_POINT ( 'NONE',  ( 0.4325450954222598288, 0.000000000000000000, 0.000000000000000000 ) ) ;
#46690=EDGE_CURVE ( 'NONE', #45742, #93240, #22442, .T. ) ;
#46719=ORIENTED_EDGE ( 'NONE', *, *, #2377, .F. ) ;
#46866=CARTESIAN_POINT ( 'NONE',  ( 20.60020833695035236, 1.530808498934189845E-16, -1.249999999999998446 ) ) ;
#46919=CARTESIAN_POINT ( 'NONE',  ( 20.60020833695035236, 0.000000000000000000, 0.000000000000000000 ) ) ;
#46966=CARTESIAN_POINT ( 'NONE',  ( 2.230654205607476293, 0.1647943925233646134, -7.514475724998474108E-17 ) ) ;
#47237=PRODUCT_DEFINITION_FORMATION_WITH_SPECIFIED_SOURCE ( 'ANY', '', #28832, .NOT_KNOWN. ) ;
#47547=ORIENTED_EDGE ( 'NONE', *, *, #1322, .T. ) ;
#47655=AXIS2_PLACEMENT_3D ( 'NONE', #45941, #53058, #75869 ) ;
#47979=AXIS2_PLACEMENT_3D ( 'NONE', #48532, #57643, #40902 ) ;
#48022=DIRECTION ( 'NONE',  ( -0.5656310827093757876, -0.8246584009594636333, -1.161164194647626387E-16 ) ) ;
#48033=CARTESIAN_POINT ( 'NONE',  ( 1.949999999999999956, -0.1925000000000001155, -0.1925000000000000600 ) ) ;
#48160=CYLINDRICAL_SURFACE ( 'NONE', #26518, 1.249999999999997113 ) ;
#48472=AXIS2_PLACEMENT_3D ( 'NONE', #11976, #82481, #43443 ) ;
#48532=CARTESIAN_POINT ( 'NONE',  ( 2.100208336950355914, 0.000000000000000000, 0.000000000000000000 ) ) ;
#48672=DIRECTION ( 'NONE',  ( 0.000000000000000000, 0.000000000000000000, 1.000000000000000000 ) ) ;
#49066=VERTEX_POINT ( 'NONE', #4300 ) ;
#49125=SPHERICAL_SURFACE ( 'NONE', #75113, 6.600000000000001421 ) ;
#49176=FACE_OUTER_BOUND ( 'NONE', #68474, .T. ) ;
#49304=DIRECTION ( 'NONE',  ( -0.09824042138329590335, 4.470611911092166224E-17, -0.9951627101165078093 ) ) ;
#49459=FACE_OUTER_BOUND ( 'NONE', #76697, .T. ) ;
#49549=EDGE_CURVE ( 'NONE', #29476, #71994, #72021, .T. ) ;
#49668=DIRECTION ( 'NONE',  ( 0.5656310827093757876, -2.995395837334947501E-15, 0.8246584009594636333 ) ) ;
#49922=PLANE ( 'NONE',  #11120 ) ;
#50151=AXIS2_PLACEMENT_3D ( 'NONE', #42574, #88741, #35941 ) ;
#50873=CIRCLE ( 'NONE', #19916, 2.350000000000000089 ) ;
#50939=ORIENTED_EDGE ( 'NONE', *, *, #4885, .F. ) ;
#50960=ORIENTED_EDGE ( 'NONE', *, *, #4885, .T. ) ;
#51241=AXIS2_PLACEMENT_3D ( 'NONE', #46919, #54533, #33189 ) ;
#52201=VERTEX_POINT ( 'NONE', #21228 ) ;
#52527=CARTESIAN_POINT ( 'NONE',  ( 2.246611357655420083, -0.1632191352058117717, 0.1632191352058111888 ) ) ;
#52640=FACE_OUTER_BOUND ( 'NONE', #36326, .T. ) ;
#52976=CARTESIAN_POINT ( 'NONE',  ( 0.000000000000000000, 1.530000000000000027, 0.3849999999999992872 ) ) ;
#53058=DIRECTION ( 'NONE',  ( -1.000000000000000000, -0.000000000000000000, -0.000000000000000000 ) ) ;
#53404=DIRECTION ( 'NONE',  ( -1.000000000000000000, -0.000000000000000000, -0.000000000000000000 ) ) ;
#53593=PLANE ( 'NONE',  #60986 ) ;
#53606=VERTEX_POINT ( 'NONE', #10598 ) ;
#53855=DIRECTION ( 'NONE',  ( -1.000000000000000000, -0.000000000000000000, -0.000000000000000000 ) ) ;
#53862=CARTESIAN_POINT ( 'NONE',  ( 0.02224039135773590858, 0.3828044741864786715, 0.3828044741864790046 ) ) ;
#53906=ORIENTED_EDGE ( 'NONE', *, *, #27935, .T. ) ;
#54016=CARTESIAN_POINT ( 'NONE',  ( 2.100208336950355914, 0.000000000000000000, 0.000000000000000000 ) ) ;
#54207=DIRECTION ( 'NONE',  ( 0.8219392559241306406, -0.5637660281018075370, 0.08114015731558719968 ) ) ;
#54220=CARTESIAN_POINT ( 'NONE',  ( 0.1645010273463760886, 0.3687607960183654776, 1.417169167140628794 ) ) ;
#54243=DIRECTION ( 'NONE',  ( 0.000000000000000000, 0.000000000000000000, 1.000000000000000000 ) ) ;
#54358=AXIS2_PLACEMENT_3D ( 'NONE', #26457, #49304, #4117 ) ;
#54421=CARTESIAN_POINT ( 'NONE',  ( 6.573941812937369455, 1.185825954564562440E-17, -0.2639660507643281639 ) ) ;
#54533=DIRECTION ( 'NONE',  ( -1.000000000000000000, -0.000000000000000000, -0.000000000000000000 ) ) ;
#54742=FACE_OUTER_BOUND ( 'NONE', #87914, .T. ) ;
#54782=DIRECTION ( 'NONE',  ( 0.9951627101165076983, -0.09824042138329622254, -3.430045979798646929E-16 ) ) ;
#54937=DIRECTION ( 'NONE',  ( -1.000000000000000000, -0.000000000000000000, -0.000000000000000000 ) ) ;
#54977=ADVANCED_BREP_SHAPE_REPRESENTATION ( '', ( #42411, #37391 ), #16366 ) ;
#55106=ORIENTED_EDGE ( 'NONE', *, *, #63217, .T. ) ;
#55511=AXIS2_PLACEMENT_3D ( 'NONE', #32366, #32876, #63341 ) ;
#56049=DIRECTION ( 'NONE',  ( -1.000000000000000000, -0.000000000000000000, -0.000000000000000000 ) ) ;
#56174=DIRECTION ( 'NONE',  ( 0.8219392559241307517, -0.08114015731558921196, 0.5637660281018073150 ) ) ;
#56179=CIRCLE ( 'NONE', #36669, 1.249999999999998446 ) ;
#56191=ORIENTED_EDGE ( 'NONE', *, *, #64285, .T. ) ;
#56472=AXIS2_PLACEMENT_3D ( 'NONE', #94441, #73616, #80224 ) ;
#56597=PLANE ( 'NONE',  #96764 ) ;
#56608=ORIENTED_EDGE ( 'NONE', *, *, #44426, .T. ) ;
#56695=VERTEX_POINT ( 'NONE', #19679 ) ;
#56715=CARTESIAN_POINT ( 'NONE',  ( 2.100208336950355914, 0.000000000000000000, 1.249999999999996003 ) ) ;
#56901=DIRECTION ( 'NONE',  ( 0.09824042138329625029, 2.980407940728111021E-17, -0.9951627101165079203 ) ) ;
#56949=EDGE_LOOP ( 'NONE', ( #87107, #92854, #98610 ) ) ;
#57157=LINE ( 'NONE', #58147, #84027 ) ;
#57317=CIRCLE ( 'NONE', #39477, 6.594667762285751245 ) ;
#57390=EDGE_LOOP ( 'NONE', ( #189, #8247, #8521 ) ) ;
#57421=PLANE ( 'NONE',  #33269 ) ;
#57582=CARTESIAN_POINT ( 'NONE',  ( 0.4325450954222598288, 0.000000000000000000, 2.350000000000000089 ) ) ;
#57643=DIRECTION ( 'NONE',  ( -1.000000000000000000, -0.000000000000000000, -0.000000000000000000 ) ) ;
#57732=FACE_OUTER_BOUND ( 'NONE', #33536, .T. ) ;
#57737=ORIENTED_EDGE ( 'NONE', *, *, #21854, .T. ) ;
#57903=CARTESIAN_POINT ( 'NONE',  ( 0.000000000000000000, -1.530000000000000027, 0.3849999999999990652 ) ) ;
#58038=ORIENTED_EDGE ( 'NONE', *, *, #75686, .F. ) ;
#58050=EDGE_CURVE ( 'NONE', #72919, #29476, #22870, .T. ) ;
#58147=CARTESIAN_POINT ( 'NONE',  ( -15.87499999999997868, 2.877919977996279334E-16, -2.349999999999999645 ) ) ;
#58200=EDGE_LOOP ( 'NONE', ( #76391, #27386 ) ) ;
#58233=CARTESIAN_POINT ( 'NONE',  ( 0.4325450954222598288, 0.000000000000000000, 0.000000000000000000 ) ) ;
#58272=VECTOR ( 'NONE', #22601, 1000.000000000000000 ) ;
#58601=ORIENTED_EDGE ( 'NONE', *, *, #62334, .T. ) ;
#58694=LINE ( 'NONE', #56715, #30865 ) ;
#58851=CARTESIAN_POINT ( 'NONE',  ( 2.246611357655420083, 0.1632191352058117717, -0.1632191352058112166 ) ) ;
#59166=DIRECTION ( 'NONE',  ( 0.09824042138329625029, 0.9951627101165079203, 3.504396110891627214E-15 ) ) ;
#59246=ORIENTED_EDGE ( 'NONE', *, *, #46363, .T. ) ;
#59346=DIRECTION ( 'NONE',  ( 0.9903949459893286456, -0.09776975748869043414, 0.09776975748869007332 ) ) ;
#59388=DIRECTION ( 'NONE',  ( 0.000000000000000000, -1.000000000000000000, -1.224646799147353207E-16 ) ) ;
#59414=EDGE_CURVE ( 'NONE', #71994, #87941, #86862, .T. ) ;
#59487=ORIENTED_EDGE ( 'NONE', *, *, #86747, .F. ) ;
#59651=ORIENTED_EDGE ( 'NONE', *, *, #70339, .F. ) ;
#59687=VERTEX_POINT ( 'NONE', #54220 ) ;
#59777=ORIENTED_EDGE ( 'NONE', *, *, #3284, .F. ) ;
#59944=ADVANCED_FACE ( 'NONE', ( #49459 ), #18488, .T. ) ;
#60556=ORIENTED_EDGE ( 'NONE', *, *, #64503, .F. ) ;
#60602=DIRECTION ( 'NONE',  ( -1.000000000000000000, 0.000000000000000000, 0.000000000000000000 ) ) ;
#60986=AXIS2_PLACEMENT_3D ( 'NONE', #46966, #30226, #8393 ) ;
#61075=CARTESIAN_POINT ( 'NONE',  ( 0.000000000000000000, 0.3849999999999945688, 1.530000000000001359 ) ) ;
#61161=ORIENTED_EDGE ( 'NONE', *, *, #26653, .T. ) ;
#61333=ORIENTED_EDGE ( 'NONE', *, *, #43858, .T. ) ;
#61764=DIRECTION ( 'NONE',  ( 0.9951627101165076983, 0.000000000000000000, 0.09824042138329622254 ) ) ;
#62334=EDGE_CURVE ( 'NONE', #8243, #31435, #6040, .T. ) ;
#62420=ORIENTED_EDGE ( 'NONE', *, *, #21614, .F. ) ;
#63084=PLANE ( 'NONE',  #30789 ) ;
#63217=EDGE_CURVE ( 'NONE', #96655, #18999, #97406, .T. ) ;
#63341=DIRECTION ( 'NONE',  ( -0.9951627101165076983, 0.000000000000000000, 0.09824042138329588947 ) ) ;
#63447=DIRECTION ( 'NONE',  ( 0.000000000000000000, 0.000000000000000000, 1.000000000000000000 ) ) ;
#63639=ORIENTED_EDGE ( 'NONE', *, *, #76912, .F. ) ;
#63799=LINE ( 'NONE', #25198, #23840 ) ;
#64101=VECTOR ( 'NONE', #69267, 1000.000000000000114 ) ;
#64165=AXIS2_PLACEMENT_3D ( 'NONE', #99433, #76589, #45663 ) ;
#64285=EDGE_CURVE ( 'NONE', #29436, #41575, #93671, .T. ) ;
#64427=CARTESIAN_POINT ( 'NONE',  ( 2.100208336950355914, 1.530808498934186394E-16, -1.249999999999996003 ) ) ;
#64458=FACE_OUTER_BOUND ( 'NONE', #58200, .T. ) ;
#64503=EDGE_CURVE ( 'NONE', #49066, #52201, #12694, .T. ) ;
#64691=ORIENTED_EDGE ( 'NONE', *, *, #72028, .T. ) ;
#64703=ADVANCED_FACE ( 'NONE', ( #25313 ), #10091, .T. ) ;
#64988=ADVANCED_FACE ( 'NONE', ( #27812 ), #33426, .F. ) ;
#65121=ORIENTED_EDGE ( 'NONE', *, *, #2377, .T. ) ;
#65325=ORIENTED_EDGE ( 'NONE', *, *, #1322, .F. ) ;
#65867=DIRECTION ( 'NONE',  ( -0.5656310827093757876, -0.8246584009594636333, -1.161164194647626387E-16 ) ) ;
#65973=VECTOR ( 'NONE', #39348, 1000.000000000000227 ) ;
#66299=CIRCLE ( 'NONE', #48472, 6.119803529381341534 ) ;
#66612=DIRECTION ( 'NONE',  ( -0.5656310827093756766, 0.8246584009594636333, 1.161164194647626880E-16 ) ) ;
#66686=CARTESIAN_POINT ( 'NONE',  ( 2.100208336950355914, 0.000000000000000000, 1.249999999999996003 ) ) ;
#66729=CARTESIAN_POINT ( 'NONE',  ( 6.600000000000001421, 0.000000000000000000, 0.000000000000000000 ) ) ;
#66768=EDGE_CURVE ( 'NONE', #76458, #44866, #16462, .T. ) ;
#67011=DIRECTION ( 'NONE',  ( -0.9951627101165078093, -0.09824042138329590335, 0.000000000000000000 ) ) ;
#67021=CIRCLE ( 'NONE', #71866, 6.594667762285749468 ) ;
#67109=ORIENTED_EDGE ( 'NONE', *, *, #37866, .T. ) ;
#67507=ORIENTED_EDGE ( 'NONE', *, *, #18968, .T. ) ;
#67830=ADVANCED_FACE ( 'NONE', ( #70499 ), #38042, .T. ) ;
#68474=EDGE_LOOP ( 'NONE', ( #88889, #57737, #91101, #24303 ) ) ;
#68487=AXIS2_PLACEMENT_3D ( 'NONE', #6671, #15782, #29505 ) ;
#68805=CARTESIAN_POINT ( 'NONE',  ( 1.949999999999999956, -0.1925000000000001155, -0.1925000000000000600 ) ) ;
#68842=AXIS2_PLACEMENT_3D ( 'NONE', #1368, #42803, #40917 ) ;
#68937=ORIENTED_EDGE ( 'NONE', *, *, #16769, .F. ) ;
#69267=DIRECTION ( 'NONE',  ( 0.8219392559241307517, 0.5637660281018075370, 0.08114015731558725519 ) ) ;
#69361=PLANE ( 'NONE',  #76467 ) ;
#69414=ORIENTED_EDGE ( 'NONE', *, *, #9691, .T. ) ;
#69653=ORIENTED_EDGE ( 'NONE', *, *, #34187, .T. ) ;
#69854=CARTESIAN_POINT ( 'NONE',  ( 5.202077965628057576, -2.038091937962834166, -2.869745073849994963E-16 ) ) ;
#70339=EDGE_CURVE ( 'NONE', #18921, #10125, #89106, .T. ) ;
#70499=FACE_OUTER_BOUND ( 'NONE', #11244, .T. ) ;
#71261=CARTESIAN_POINT ( 'NONE',  ( -15.87499999999997868, 0.000000000000000000, 0.000000000000000000 ) ) ;
#71263=CIRCLE ( 'NONE', #33966, 6.119803529381342422 ) ;
#71312=ORIENTED_EDGE ( 'NONE', *, *, #40541, .F. ) ;
#71364=EDGE_CURVE ( 'NONE', #93240, #87941, #58694, .T. ) ;
#71403=ORIENTED_EDGE ( 'NONE', *, *, #20018, .T. ) ;
#71764=CIRCLE ( 'NONE', #94427, 6.594667762285751245 ) ;
#71866=AXIS2_PLACEMENT_3D ( 'NONE', #19308, #36037, #67011 ) ;
#71957=CARTESIAN_POINT ( 'NONE',  ( 6.600000000000001421, 0.000000000000000000, 0.000000000000000000 ) ) ;
#71994=VERTEX_POINT ( 'NONE', #934 ) ;
#72021=LINE ( 'NONE', #64427, #36339 ) ;
#72028=EDGE_CURVE ( 'NONE', #87941, #36724, #78536, .T. ) ;
#72257=AXIS2_PLACEMENT_3D ( 'NONE', #12795, #74698, #4705 ) ;
#72432=DIRECTION ( 'NONE',  ( -0.7071067811865452413, 0.000000000000000000, 0.7071067811865497932 ) ) ;
#72919=VERTEX_POINT ( 'NONE', #46866 ) ;
#72961=CIRCLE ( 'NONE', #28963, 2.350000000000000089 ) ;
#73491=ORIENTED_EDGE ( 'NONE', *, *, #34187, .F. ) ;
#73593=DIRECTION ( 'NONE',  ( -1.000000000000000000, -0.000000000000000000, -0.000000000000000000 ) ) ;
#73616=DIRECTION ( 'NONE',  ( 0.09824042138329590335, -0.9951627101165079203, -3.519298150595267883E-15 ) ) ;
#73982=CARTESIAN_POINT ( 'NONE',  ( 0.02224039135773677595, -0.3828044741864776723, -0.3828044741864797262 ) ) ;
#74698=DIRECTION ( 'NONE',  ( -1.000000000000000000, -0.000000000000000000, -0.000000000000000000 ) ) ;
#74849=DIRECTION ( 'NONE',  ( 0.9903949459893287566, 0.09776975748869010108, -0.09776975748868974025 ) ) ;
#74910=ORIENTED_EDGE ( 'NONE', *, *, #86747, .T. ) ;
#74920=DIRECTION ( 'NONE',  ( -1.000000000000000000, -0.000000000000000000, -0.000000000000000000 ) ) ;
#75113=AXIS2_PLACEMENT_3D ( 'NONE', #71957, #94773, #18152 ) ;
#75216=ORIENTED_EDGE ( 'NONE', *, *, #46690, .T. ) ;
#75262=DIRECTION ( 'NONE',  ( 0.8219392559241306406, 0.08114015731558892053, -0.5637660281018073150 ) ) ;
#75319=ADVANCED_FACE ( 'NONE', ( #52640 ), #69361, .T. ) ;
#75444=FACE_OUTER_BOUND ( 'NONE', #9157, .T. ) ;
#75509=ADVANCED_FACE ( 'NONE', ( #91685 ), #79968, .F. ) ;
#75515=EDGE_LOOP ( 'NONE', ( #42499, #69414, #59651 ) ) ;
#75686=EDGE_CURVE ( 'NONE', #35831, #56695, #98001, .T. ) ;
#75869=DIRECTION ( 'NONE',  ( 0.000000000000000000, 0.000000000000000000, 1.000000000000000000 ) ) ;
#76391=ORIENTED_EDGE ( 'NONE', *, *, #18968, .F. ) ;
#76455=DIRECTION ( 'NONE',  ( -0.09824042138329623641, -2.980407940728110405E-17, 0.9951627101165078093 ) ) ;
#76458=VERTEX_POINT ( 'NONE', #91039 ) ;
#76467=AXIS2_PLACEMENT_3D ( 'NONE', #7954, #76455, #61764 ) ;
#76589=DIRECTION ( 'NONE',  ( -1.000000000000000000, -0.000000000000000000, -0.000000000000000000 ) ) ;
#76697=EDGE_LOOP ( 'NONE', ( #2714, #74910, #71312, #68937, #33068 ) ) ;
#76912=EDGE_CURVE ( 'NONE', #8243, #36724, #40925, .T. ) ;
#76915=ORIENTED_EDGE ( 'NONE', *, *, #10129, .T. ) ;
#77040=DIRECTION ( 'NONE',  ( -1.000000000000000000, -0.000000000000000000, -0.000000000000000000 ) ) ;
#77091=VERTEX_POINT ( 'NONE', #90308 ) ;
#77315=DIRECTION ( 'NONE',  ( 0.09824042138329625029, 2.980407940728111021E-17, -0.9951627101165079203 ) ) ;
#77397=ORIENTED_EDGE ( 'NONE', *, *, #11905, .F. ) ;
#77586=DIRECTION ( 'NONE',  ( -0.09824042138329623641, -0.9951627101165078093, -3.504396110891626425E-15 ) ) ;
#78183=CARTESIAN_POINT ( 'NONE',  ( 0.4325450954222598288, 0.000000000000000000, 0.000000000000000000 ) ) ;
#78206=EDGE_CURVE ( 'NONE', #86377, #77091, #67021, .T. ) ;
#78306=ADVANCED_FACE ( 'NONE', ( #87207 ), #48160, .T. ) ;
#78311=DIRECTION ( 'NONE',  ( -1.000000000000000000, -0.000000000000000000, -0.000000000000000000 ) ) ;
#78371=ORIENTED_EDGE ( 'NONE', *, *, #44426, .F. ) ;
#78523=ORIENTED_EDGE ( 'NONE', *, *, #90534, .F. ) ;
#78536=LINE ( 'NONE', #46113, #24342 ) ;
#78587=ORIENTED_EDGE ( 'NONE', *, *, #64503, .T. ) ;
#79219=CARTESIAN_POINT ( 'NONE',  ( 1.949999999999999956, 0.1924999999999999489, 0.1925000000000000044 ) ) ;
#79432=EDGE_CURVE ( 'NONE', #44866, #56695, #93620, .T. ) ;
#79460=CARTESIAN_POINT ( 'NONE',  ( 0.02224039135773590858, -0.3828044741864804479, 0.3828044741864790601 ) ) ;
#79474=( LENGTH_UNIT ( ) NAMED_UNIT ( * ) SI_UNIT ( .MILLI., .METRE. ) );
#79638=PLANE ( 'NONE',  #36662 ) ;
#79725=FACE_OUTER_BOUND ( 'NONE', #32968, .T. ) ;
#79968=PLANE ( 'NONE',  #99143 ) ;
#80224=DIRECTION ( 'NONE',  ( -0.9951627101165078093, -0.09824042138329590335, -1.421085471520200214E-14 ) ) ;
#80233=CARTESIAN_POINT ( 'NONE',  ( 1.949999999999999956, 0.1925000000000000044, -0.1925000000000000600 ) ) ;
#80947=ORIENTED_EDGE ( 'NONE', *, *, #46690, .F. ) ;
#81227=EDGE_CURVE ( 'NONE', #76458, #31435, #90773, .T. ) ;
#81318=CARTESIAN_POINT ( 'NONE',  ( 2.100208336950355914, 2.204364238465233111E-16, -1.249999999999996003 ) ) ;
#81347=( NAMED_UNIT ( * ) PLANE_ANGLE_UNIT ( ) SI_UNIT ( $, .RADIAN. ) );
#81636=LINE ( 'NONE', #19716, #88550 ) ;
#81827=ORIENTED_EDGE ( 'NONE', *, *, #75686, .T. ) ;
#82481=DIRECTION ( 'NONE',  ( -0.5656310827093756766, -2.995395837334948290E-15, 0.8246584009594636333 ) ) ;
#83055=PLANE ( 'NONE',  #29912 ) ;
#83483=CARTESIAN_POINT ( 'NONE',  ( 5.202077965628057576, 2.038091937962834166, 2.869745073849996442E-16 ) ) ;
#83863=DIRECTION ( 'NONE',  ( -0.9951627101165078093, 1.776356839400250267E-15, 0.09824042138329590335 ) ) ;
#83912=CARTESIAN_POINT ( 'NONE',  ( 6.573941812937369455, 1.185825954564562440E-17, -0.2639660507643281639 ) ) ;
#84027=VECTOR ( 'NONE', #19563, 1000.000000000000000 ) ;
#84281=CARTESIAN_POINT ( 'NONE',  ( 1.949999999999999956, 0.1924999999999999489, 0.1925000000000000044 ) ) ;
#84937=CARTESIAN_POINT ( 'NONE',  ( 6.573941812937369455, -7.905506363763796338E-18, 0.2639660507643297183 ) ) ;
#85500=CARTESIAN_POINT ( 'NONE',  ( 1.000208336950358934, 0.000000000000000000, 2.349999999999999645 ) ) ;
#85867=EDGE_LOOP ( 'NONE', ( #40967, #46346, #75216, #3599 ) ) ;
#85907=ORIENTED_EDGE ( 'NONE', *, *, #64285, .F. ) ;
#85920=AXIS2_PLACEMENT_3D ( 'NONE', #4689, #66612, #97522 ) ;
#85988=CARTESIAN_POINT ( 'NONE',  ( 0.000000000000000000, -1.530000000000000027, -0.3850000000000000089 ) ) ;
#86377=VERTEX_POINT ( 'NONE', #73982 ) ;
#86655=CIRCLE ( 'NONE', #68842, 2.350000000000000089 ) ;
#86747=EDGE_CURVE ( 'NONE', #71994, #53606, #57157, .T. ) ;
#86805=VECTOR ( 'NONE', #53855, 1000.000000000000000 ) ;
#86862=CIRCLE ( 'NONE', #72257, 2.349999999999999645 ) ;
#87067=PRODUCT_DEFINITION_SHAPE ( 'NONE', 'NONE',  #14113 ) ;
#87107=ORIENTED_EDGE ( 'NONE', *, *, #9691, .F. ) ;
#87207=FACE_OUTER_BOUND ( 'NONE', #42224, .T. ) ;
#87355=CONICAL_SURFACE ( 'NONE', #98650, 1.249999999999996003, 0.7853981633974514986 ) ;
#87531=CARTESIAN_POINT ( 'NONE',  ( 2.230654205607476737, -0.1647943925233645579, -7.922169807384186089E-16 ) ) ;
#87818=DIRECTION ( 'NONE',  ( 0.000000000000000000, 0.000000000000000000, 1.000000000000000000 ) ) ;
#87835=DIRECTION ( 'NONE',  ( 0.9951627101165076983, 0.000000000000000000, 0.09824042138329622254 ) ) ;
#87899=CIRCLE ( 'NONE', #68487, 6.119803529381341534 ) ;
#87914=EDGE_LOOP ( 'NONE', ( #60556, #38357, #18361, #58601, #43967, #61333, #15813, #59777, #20499, #56608, #77397 ) ) ;
#87940=CARTESIAN_POINT ( 'NONE',  ( 0.1645010273463760886, -1.417169167140626573, 0.3687607960183696965 ) ) ;
#87941=VERTEX_POINT ( 'NONE', #85500 ) ;
#88497=ORIENTED_EDGE ( 'NONE', *, *, #46349, .F. ) ;
#88550=VECTOR ( 'NONE', #34963, 1000.000000000000000 ) ;
#88694=SHAPE_REPRESENTATION_RELATIONSHIP ( 'NONE' , 'NONE' ,  #9419, #54977 ) ;
#88741=DIRECTION ( 'NONE',  ( 0.09824042138329625029, 0.9951627101165079203, 3.504396110891627214E-15 ) ) ;
#88889=ORIENTED_EDGE ( 'NONE', *, *, #49549, .F. ) ;
#88920=VECTOR ( 'NONE', #94954, 1000.000000000000000 ) ;
#89019=ORIENTED_EDGE ( 'NONE', *, *, #94899, .T. ) ;
#89106=CIRCLE ( 'NONE', #17831, 6.594667762285749468 ) ;
#89179=CARTESIAN_POINT ( 'NONE',  ( 5.202077965628057576, -2.038091937962834166, -2.869745073849994963E-16 ) ) ;
#89461=( NAMED_UNIT ( * ) SI_UNIT ( $, .STERADIAN. ) SOLID_ANGLE_UNIT ( ) );
#89717=CARTESIAN_POINT ( 'NONE',  ( 1.949999999999999956, -0.1925000000000007261, 0.1924999999999992828 ) ) ;
#89774=ADVANCED_FACE ( 'NONE', ( #8783 ), #63084, .F. ) ;
#90032=ORIENTED_EDGE ( 'NONE', *, *, #95823, .T. ) ;
#90308=CARTESIAN_POINT ( 'NONE',  ( 0.1645010273463760886, -0.3687607960183646449, -1.417169167140628350 ) ) ;
#90534=EDGE_CURVE ( 'NONE', #53606, #8243, #72961, .T. ) ;
#90658=DIRECTION ( 'NONE',  ( 0.000000000000000000, 0.000000000000000000, 1.000000000000000000 ) ) ;
#90773=CIRCLE ( 'NONE', #85920, 6.119803529381341534 ) ;
#90978=EDGE_LOOP ( 'NONE', ( #76915, #61161, #81827, #62420 ) ) ;
#90980=DIRECTION ( 'NONE',  ( 0.09824042138329590335, -4.470611911092166224E-17, 0.9951627101165079203 ) ) ;
#91007=LINE ( 'NONE', #61075, #6069 ) ;
#91039=CARTESIAN_POINT ( 'NONE',  ( 0.1645010273463769490, -1.417169167140626129, -0.3687607960183705291 ) ) ;
#91101=ORIENTED_EDGE ( 'NONE', *, *, #71364, .T. ) ;
#91223=ORIENTED_EDGE ( 'NONE', *, *, #79432, .F. ) ;
#91375=AXIS2_PLACEMENT_3D ( 'NONE', #83483, #38806, #15467 ) ;
#91464=CARTESIAN_POINT ( 'NONE',  ( 2.230654205607476293, -6.505213034913026604E-16, -0.1647943925233646134 ) ) ;
#91685=FACE_OUTER_BOUND ( 'NONE', #2974, .T. ) ;
#92854=ORIENTED_EDGE ( 'NONE', *, *, #26653, .F. ) ;
#93031=CIRCLE ( 'NONE', #91375, 6.119803529381341534 ) ;
#93062=ORIENTED_EDGE ( 'NONE', *, *, #62334, .F. ) ;
#93125=LINE ( 'NONE', #1298, #65973 ) ;
#93240=VERTEX_POINT ( 'NONE', #66686 ) ;
#93309=CARTESIAN_POINT ( 'NONE',  ( -15.87499999999997868, 0.000000000000000000, 0.000000000000000000 ) ) ;
#93620=LINE ( 'NONE', #68805, #58272 ) ;
#93663=VECTOR ( 'NONE', #75262, 1000.000000000000227 ) ;
#93671=CIRCLE ( 'NONE', #56472, 6.594667762285749468 ) ;
#93958=ADVANCED_FACE ( 'NONE', ( #64458 ), #79638, .F. ) ;
#94427=AXIS2_PLACEMENT_3D ( 'NONE', #84937, #77315, #7816 ) ;
#94441=CARTESIAN_POINT ( 'NONE',  ( 6.573941812937369455, 0.2639660507643281639, 9.334907998774166978E-16 ) ) ;
#94590=CYLINDRICAL_SURFACE ( 'NONE', #2794, 1.249999999999997113 ) ;
#94691=DIRECTION ( 'NONE',  ( 0.8246584009594636333, 0.5656310827093757876, 0.000000000000000000 ) ) ;
#94773=DIRECTION ( 'NONE',  ( 0.000000000000000000, 0.000000000000000000, 1.000000000000000000 ) ) ;
#94899=EDGE_CURVE ( 'NONE', #93240, #29476, #35009, .T. ) ;
#94954=DIRECTION ( 'NONE',  ( 0.000000000000000000, 1.408054769461693696E-16, -1.000000000000000000 ) ) ;
#94970=CIRCLE ( 'NONE', #51241, 1.249999999999998446 ) ;
#95076=ADVANCED_FACE ( 'NONE', ( #45406 ), #87355, .T. ) ;
#95199=DIRECTION ( 'NONE',  ( 0.5656310827093757876, -0.8246584009594636333, -1.161164194647627127E-16 ) ) ;
#95347=AXIS2_PLACEMENT_3D ( 'NONE', #35559, #5594, #59388 ) ;
#95572=DIRECTION ( 'NONE',  ( -0.9951627101165076983, -0.09824042138329588947, -3.430045979798635096E-16 ) ) ;
#95823=EDGE_CURVE ( 'NONE', #41575, #56695, #12949, .T. ) ;
#96239=ORIENTED_EDGE ( 'NONE', *, *, #45417, .F. ) ;
#96288=CARTESIAN_POINT ( 'NONE',  ( 20.60020833695035236, 0.000000000000000000, 1.249999999999998446 ) ) ;
#96457=DIRECTION ( 'NONE',  ( 0.000000000000000000, 0.000000000000000000, 1.000000000000000000 ) ) ;
#96655=VERTEX_POINT ( 'NONE', #23823 ) ;
#96764=AXIS2_PLACEMENT_3D ( 'NONE', #87531, #26632, #27634 ) ;
#96962=EDGE_CURVE ( 'NONE', #12764, #96655, #24199, .T. ) ;
#97157=LINE ( 'NONE', #11916, #27995 ) ;
#97406=LINE ( 'NONE', #58851, #1268 ) ;
#97522=DIRECTION ( 'NONE',  ( 0.8246584009594635223, 0.5656310827093757876, 2.309263891220325920E-14 ) ) ;
#98001=LINE ( 'NONE', #84281, #6801 ) ;
#98063=VERTEX_POINT ( 'NONE', #87940 ) ;
#98202=CARTESIAN_POINT ( 'NONE',  ( 6.573941812937369455, -0.2639660507643297183, -9.295380466955404257E-16 ) ) ;
#98610=ORIENTED_EDGE ( 'NONE', *, *, #4247, .F. ) ;
#98615=DIRECTION ( 'NONE',  ( 0.8219392559241306406, -0.08114015731558522904, -0.5637660281018079811 ) ) ;
#98650=AXIS2_PLACEMENT_3D ( 'NONE', #54016, #6824, #99654 ) ;
#98787=DIRECTION ( 'NONE',  ( 0.5656310827093757876, 0.8246584009594636333, 1.161164194647626634E-16 ) ) ;
#99143=AXIS2_PLACEMENT_3D ( 'NONE', #48033, #95199, #94691 ) ;
#99433=CARTESIAN_POINT ( 'NONE',  ( -15.87499999999997868, 0.000000000000000000, 0.000000000000000000 ) ) ;
#99654=DIRECTION ( 'NONE',  ( 0.000000000000000000, 0.000000000000000000, 1.000000000000000000 ) ) ;
#100434=COLOUR_RGB('Deep Blue', 0.66274510, 0.83137255, 0.94901961);
#100435=FILL_AREA_STYLE_COLOUR('',#100434);
#100436=FILL_AREA_STYLE('',(#100435));
#100437=SURFACE_STYLE_FILL_AREA(#100436);
#100438=SURFACE_SIDE_STYLE('',(#100437));
#100439=SURFACE_STYLE_USAGE(.BOTH.,#100438);
#100440=PRESENTATION_STYLE_ASSIGNMENT((#100439));
#100490=STYLED_ITEM('',(#100440),#42411);
#100491=MECHANICAL_DESIGN_GEOMETRIC_PRESENTATION_REPRESENTATION('',(#100490),#16366);
ENDSEC;
END-ISO-10303-21;
